ISO-10303-21;
HEADER;
/* Generated by software containing ST-Developer
 * from STEP Tools, Inc. (www.steptools.com) 
 */

FILE_DESCRIPTION(
/* description */ (''),
/* implementation_level */ '2;1');

FILE_NAME(
/* name */ 'Left_Block.step',
/* time_stamp */ '2026-10-23T22:29:29+06:00',
/* author */ (''),
/* organization */ (''),
/* preprocessor_version */ 'ST-DEVELOPER v20.2',
/* originating_system */ 'Autodesk Translation Framework v15.15.0.0',
/* authorisation */ '');

FILE_SCHEMA (('AUTOMOTIVE_DESIGN { 1 0 10303 214 3 1 1 }'));
ENDSEC;

DATA;
#10=MECHANICAL_DESIGN_GEOMETRIC_PRESENTATION_REPRESENTATION('',(#77),#7047);
#57=SHAPE_REPRESENTATION_RELATIONSHIP('SRR','None',#7090,#67);
#67=ADVANCED_BREP_SHAPE_REPRESENTATION('',(#90),#7042);
#77=STYLED_ITEM('',(#7177),#90);
#90=MANIFOLD_SOLID_BREP('Left_Block',#3402);
#115=FACE_BOUND('',#590,.T.);
#116=FACE_BOUND('',#593,.T.);
#199=PLANE('',#3781);
#200=PLANE('',#3782);
#201=PLANE('',#3783);
#202=PLANE('',#3784);
#203=PLANE('',#3785);
#204=PLANE('',#3789);
#205=PLANE('',#3790);
#206=PLANE('',#3791);
#207=PLANE('',#3792);
#208=PLANE('',#3793);
#209=PLANE('',#3794);
#210=PLANE('',#3795);
#211=PLANE('',#3796);
#212=PLANE('',#3798);
#213=PLANE('',#3802);
#214=PLANE('',#3803);
#215=PLANE('',#3805);
#216=PLANE('',#3806);
#217=PLANE('',#3808);
#218=PLANE('',#3809);
#378=FACE_OUTER_BOUND('',#575,.T.);
#379=FACE_OUTER_BOUND('',#576,.T.);
#380=FACE_OUTER_BOUND('',#577,.T.);
#381=FACE_OUTER_BOUND('',#578,.T.);
#382=FACE_OUTER_BOUND('',#579,.T.);
#383=FACE_OUTER_BOUND('',#580,.T.);
#384=FACE_OUTER_BOUND('',#581,.T.);
#385=FACE_OUTER_BOUND('',#582,.T.);
#386=FACE_OUTER_BOUND('',#583,.T.);
#387=FACE_OUTER_BOUND('',#584,.T.);
#388=FACE_OUTER_BOUND('',#585,.T.);
#389=FACE_OUTER_BOUND('',#586,.T.);
#390=FACE_OUTER_BOUND('',#587,.T.);
#391=FACE_OUTER_BOUND('',#588,.T.);
#392=FACE_OUTER_BOUND('',#589,.T.);
#393=FACE_OUTER_BOUND('',#591,.T.);
#394=FACE_OUTER_BOUND('',#592,.T.);
#395=FACE_OUTER_BOUND('',#594,.T.);
#396=FACE_OUTER_BOUND('',#595,.T.);
#397=FACE_OUTER_BOUND('',#596,.T.);
#398=FACE_OUTER_BOUND('',#597,.T.);
#399=FACE_OUTER_BOUND('',#598,.T.);
#400=FACE_OUTER_BOUND('',#599,.T.);
#575=EDGE_LOOP('',(#2785,#2786,#2787,#2788));
#576=EDGE_LOOP('',(#2789,#2790,#2791,#2792));
#577=EDGE_LOOP('',(#2793,#2794,#2795,#2796));
#578=EDGE_LOOP('',(#2797,#2798,#2799,#2800));
#579=EDGE_LOOP('',(#2801,#2802,#2803,#2804,#2805,#2806,#2807,#2808));
#580=EDGE_LOOP('',(#2809,#2810,#2811,#2812));
#581=EDGE_LOOP('',(#2813,#2814,#2815,#2816));
#582=EDGE_LOOP('',(#2817,#2818,#2819,#2820));
#583=EDGE_LOOP('',(#2821,#2822,#2823,#2824));
#584=EDGE_LOOP('',(#2825,#2826,#2827,#2828,#2829,#2830));
#585=EDGE_LOOP('',(#2831,#2832,#2833,#2834));
#586=EDGE_LOOP('',(#2835,#2836,#2837,#2838));
#587=EDGE_LOOP('',(#2839,#2840,#2841,#2842));
#588=EDGE_LOOP('',(#2843,#2844,#2845,#2846,#2847));
#589=EDGE_LOOP('',(#2848,#2849,#2850,#2851));
#590=EDGE_LOOP('',(#2852));
#591=EDGE_LOOP('',(#2853,#2854,#2855,#2856));
#592=EDGE_LOOP('',(#2857,#2858,#2859,#2860));
#593=EDGE_LOOP('',(#2861));
#594=EDGE_LOOP('',(#2862,#2863,#2864,#2865,#2866,#2867,#2868,#2869,#2870,
#2871,#2872,#2873,#2874,#2875,#2876,#2877));
#595=EDGE_LOOP('',(#2878,#2879,#2880,#2881));
#596=EDGE_LOOP('',(#2882,#2883,#2884,#2885,#2886,#2887,#2888,#2889,#2890,
#2891,#2892,#2893,#2894,#2895));
#597=EDGE_LOOP('',(#2896,#2897,#2898,#2899));
#598=EDGE_LOOP('',(#2900,#2901,#2902,#2903));
#599=EDGE_LOOP('',(#2904,#2905,#2906,#2907,#2908));
#774=CIRCLE('',#3787,2.5);
#775=CIRCLE('',#3788,2.5);
#776=CIRCLE('',#3797,4.99999999999999);
#777=CIRCLE('',#3800,4.99999999999999);
#778=CIRCLE('',#3801,4.99999999999999);
#779=CIRCLE('',#3804,4.99999999999999);
#949=LINE('',#5746,#1243);
#950=LINE('',#5748,#1244);
#951=LINE('',#5750,#1245);
#952=LINE('',#5751,#1246);
#953=LINE('',#5754,#1247);
#954=LINE('',#5756,#1248);
#955=LINE('',#5757,#1249);
#956=LINE('',#5760,#1250);
#957=LINE('',#5762,#1251);
#958=LINE('',#5763,#1252);
#959=LINE('',#5765,#1253);
#960=LINE('',#5768,#1254);
#961=LINE('',#5770,#1255);
#962=LINE('',#5772,#1256);
#963=LINE('',#5774,#1257);
#964=LINE('',#5775,#1258);
#965=LINE('',#5780,#1259);
#966=LINE('',#5785,#1260);
#967=LINE('',#5787,#1261);
#968=LINE('',#5789,#1262);
#969=LINE('',#5790,#1263);
#970=LINE('',#5794,#1264);
#971=LINE('',#5796,#1265);
#972=LINE('',#5798,#1266);
#973=LINE('',#5799,#1267);
#974=LINE('',#5801,#1268);
#975=LINE('',#5802,#1269);
#976=LINE('',#5805,#1270);
#977=LINE('',#5807,#1271);
#978=LINE('',#5809,#1272);
#979=LINE('',#5811,#1273);
#980=LINE('',#5812,#1274);
#981=LINE('',#5816,#1275);
#982=LINE('',#5818,#1276);
#983=LINE('',#5820,#1277);
#984=LINE('',#5821,#1278);
#985=LINE('',#5824,#1279);
#986=LINE('',#5826,#1280);
#987=LINE('',#5827,#1281);
#988=LINE('',#5829,#1282);
#989=LINE('',#5830,#1283);
#990=LINE('',#5836,#1284);
#991=LINE('',#5838,#1285);
#992=LINE('',#5840,#1286);
#993=LINE('',#5841,#1287);
#994=LINE('',#5848,#1288);
#995=LINE('',#5849,#1289);
#996=LINE('',#5850,#1290);
#997=LINE('',#5854,#1291);
#998=LINE('',#5855,#1292);
#999=LINE('',#5856,#1293);
#1000=LINE('',#5859,#1294);
#1001=LINE('',#5862,#1295);
#1002=LINE('',#5863,#1296);
#1003=LINE('',#5865,#1297);
#1004=LINE('',#5867,#1298);
#1243=VECTOR('',#4542,10.);
#1244=VECTOR('',#4543,10.);
#1245=VECTOR('',#4544,10.);
#1246=VECTOR('',#4545,10.);
#1247=VECTOR('',#4548,10.);
#1248=VECTOR('',#4549,10.);
#1249=VECTOR('',#4550,10.);
#1250=VECTOR('',#4553,10.);
#1251=VECTOR('',#4554,10.);
#1252=VECTOR('',#4555,10.);
#1253=VECTOR('',#4558,10.);
#1254=VECTOR('',#4561,10.);
#1255=VECTOR('',#4562,10.);
#1256=VECTOR('',#4563,10.);
#1257=VECTOR('',#4564,10.);
#1258=VECTOR('',#4565,10.);
#1259=VECTOR('',#4570,2.5);
#1260=VECTOR('',#4575,10.);
#1261=VECTOR('',#4576,10.);
#1262=VECTOR('',#4577,10.);
#1263=VECTOR('',#4578,10.);
#1264=VECTOR('',#4581,10.);
#1265=VECTOR('',#4582,10.);
#1266=VECTOR('',#4583,10.);
#1267=VECTOR('',#4584,10.);
#1268=VECTOR('',#4587,10.);
#1269=VECTOR('',#4588,10.);
#1270=VECTOR('',#4591,10.);
#1271=VECTOR('',#4592,10.);
#1272=VECTOR('',#4593,10.);
#1273=VECTOR('',#4594,10.);
#1274=VECTOR('',#4595,10.);
#1275=VECTOR('',#4598,10.);
#1276=VECTOR('',#4599,10.);
#1277=VECTOR('',#4600,10.);
#1278=VECTOR('',#4601,10.);
#1279=VECTOR('',#4604,10.);
#1280=VECTOR('',#4605,10.);
#1281=VECTOR('',#4606,10.);
#1282=VECTOR('',#4609,10.);
#1283=VECTOR('',#4610,10.);
#1284=VECTOR('',#4617,10.);
#1285=VECTOR('',#4618,10.);
#1286=VECTOR('',#4619,10.);
#1287=VECTOR('',#4620,10.);
#1288=VECTOR('',#4629,10.);
#1289=VECTOR('',#4630,10.);
#1290=VECTOR('',#4631,10.);
#1291=VECTOR('',#4634,10.);
#1292=VECTOR('',#4635,10.);
#1293=VECTOR('',#4636,10.);
#1294=VECTOR('',#4641,10.);
#1295=VECTOR('',#4644,10.);
#1296=VECTOR('',#4645,10.);
#1297=VECTOR('',#4648,10.);
#1298=VECTOR('',#4651,10.);
#1616=VERTEX_POINT('',#5744);
#1617=VERTEX_POINT('',#5745);
#1618=VERTEX_POINT('',#5747);
#1619=VERTEX_POINT('',#5749);
#1620=VERTEX_POINT('',#5753);
#1621=VERTEX_POINT('',#5755);
#1622=VERTEX_POINT('',#5759);
#1623=VERTEX_POINT('',#5761);
#1624=VERTEX_POINT('',#5767);
#1625=VERTEX_POINT('',#5769);
#1626=VERTEX_POINT('',#5771);
#1627=VERTEX_POINT('',#5773);
#1628=VERTEX_POINT('',#5777);
#1629=VERTEX_POINT('',#5779);
#1630=VERTEX_POINT('',#5783);
#1631=VERTEX_POINT('',#5784);
#1632=VERTEX_POINT('',#5786);
#1633=VERTEX_POINT('',#5788);
#1634=VERTEX_POINT('',#5792);
#1635=VERTEX_POINT('',#5793);
#1636=VERTEX_POINT('',#5795);
#1637=VERTEX_POINT('',#5797);
#1638=VERTEX_POINT('',#5804);
#1639=VERTEX_POINT('',#5806);
#1640=VERTEX_POINT('',#5808);
#1641=VERTEX_POINT('',#5810);
#1642=VERTEX_POINT('',#5814);
#1643=VERTEX_POINT('',#5815);
#1644=VERTEX_POINT('',#5817);
#1645=VERTEX_POINT('',#5819);
#1646=VERTEX_POINT('',#5823);
#1647=VERTEX_POINT('',#5825);
#1648=VERTEX_POINT('',#5834);
#1649=VERTEX_POINT('',#5835);
#1650=VERTEX_POINT('',#5837);
#1651=VERTEX_POINT('',#5839);
#1652=VERTEX_POINT('',#5846);
#1653=VERTEX_POINT('',#5847);
#1654=VERTEX_POINT('',#5852);
#1655=VERTEX_POINT('',#5853);
#1656=VERTEX_POINT('',#5861);
#2027=EDGE_CURVE('',#1616,#1617,#949,.T.);
#2028=EDGE_CURVE('',#1616,#1618,#950,.T.);
#2029=EDGE_CURVE('',#1619,#1618,#951,.T.);
#2030=EDGE_CURVE('',#1617,#1619,#952,.T.);
#2031=EDGE_CURVE('',#1617,#1620,#953,.T.);
#2032=EDGE_CURVE('',#1621,#1619,#954,.T.);
#2033=EDGE_CURVE('',#1620,#1621,#955,.T.);
#2034=EDGE_CURVE('',#1620,#1622,#956,.T.);
#2035=EDGE_CURVE('',#1623,#1621,#957,.T.);
#2036=EDGE_CURVE('',#1622,#1623,#958,.T.);
#2037=EDGE_CURVE('',#1618,#1623,#959,.T.);
#2038=EDGE_CURVE('',#1624,#1622,#960,.T.);
#2039=EDGE_CURVE('',#1625,#1624,#961,.T.);
#2040=EDGE_CURVE('',#1626,#1625,#962,.T.);
#2041=EDGE_CURVE('',#1627,#1626,#963,.T.);
#2042=EDGE_CURVE('',#1616,#1627,#964,.T.);
#2043=EDGE_CURVE('',#1628,#1628,#774,.T.);
#2044=EDGE_CURVE('',#1628,#1629,#965,.T.);
#2045=EDGE_CURVE('',#1629,#1629,#775,.T.);
#2046=EDGE_CURVE('',#1630,#1631,#966,.T.);
#2047=EDGE_CURVE('',#1632,#1630,#967,.T.);
#2048=EDGE_CURVE('',#1633,#1632,#968,.T.);
#2049=EDGE_CURVE('',#1631,#1633,#969,.T.);
#2050=EDGE_CURVE('',#1634,#1635,#970,.T.);
#2051=EDGE_CURVE('',#1636,#1634,#971,.T.);
#2052=EDGE_CURVE('',#1637,#1636,#972,.T.);
#2053=EDGE_CURVE('',#1637,#1635,#973,.T.);
#2054=EDGE_CURVE('',#1635,#1630,#974,.T.);
#2055=EDGE_CURVE('',#1632,#1637,#975,.T.);
#2056=EDGE_CURVE('',#1638,#1633,#976,.T.);
#2057=EDGE_CURVE('',#1638,#1639,#977,.T.);
#2058=EDGE_CURVE('',#1639,#1640,#978,.T.);
#2059=EDGE_CURVE('',#1640,#1641,#979,.T.);
#2060=EDGE_CURVE('',#1631,#1641,#980,.T.);
#2061=EDGE_CURVE('',#1642,#1643,#981,.T.);
#2062=EDGE_CURVE('',#1642,#1644,#982,.T.);
#2063=EDGE_CURVE('',#1645,#1644,#983,.T.);
#2064=EDGE_CURVE('',#1643,#1645,#984,.T.);
#2065=EDGE_CURVE('',#1646,#1638,#985,.T.);
#2066=EDGE_CURVE('',#1646,#1647,#986,.T.);
#2067=EDGE_CURVE('',#1647,#1639,#987,.T.);
#2068=EDGE_CURVE('',#1645,#1646,#988,.T.);
#2069=EDGE_CURVE('',#1644,#1647,#989,.T.);
#2070=EDGE_CURVE('',#1640,#1642,#776,.T.);
#2071=EDGE_CURVE('',#1648,#1649,#990,.T.);
#2072=EDGE_CURVE('',#1648,#1650,#991,.T.);
#2073=EDGE_CURVE('',#1651,#1650,#992,.T.);
#2074=EDGE_CURVE('',#1649,#1651,#993,.T.);
#2075=EDGE_CURVE('',#1650,#1634,#777,.T.);
#2076=EDGE_CURVE('',#1636,#1648,#778,.T.);
#2077=EDGE_CURVE('',#1652,#1653,#994,.T.);
#2078=EDGE_CURVE('',#1627,#1653,#995,.T.);
#2079=EDGE_CURVE('',#1652,#1626,#996,.T.);
#2080=EDGE_CURVE('',#1654,#1655,#997,.T.);
#2081=EDGE_CURVE('',#1655,#1624,#998,.T.);
#2082=EDGE_CURVE('',#1653,#1651,#999,.T.);
#2083=EDGE_CURVE('',#1641,#1654,#779,.T.);
#2084=EDGE_CURVE('',#1649,#1652,#1000,.T.);
#2085=EDGE_CURVE('',#1656,#1643,#1001,.T.);
#2086=EDGE_CURVE('',#1625,#1656,#1002,.T.);
#2087=EDGE_CURVE('',#1642,#1654,#1003,.T.);
#2088=EDGE_CURVE('',#1655,#1656,#1004,.T.);
#2785=ORIENTED_EDGE('',*,*,#2027,.F.);
#2786=ORIENTED_EDGE('',*,*,#2028,.T.);
#2787=ORIENTED_EDGE('',*,*,#2029,.F.);
#2788=ORIENTED_EDGE('',*,*,#2030,.F.);
#2789=ORIENTED_EDGE('',*,*,#2031,.F.);
#2790=ORIENTED_EDGE('',*,*,#2030,.T.);
#2791=ORIENTED_EDGE('',*,*,#2032,.F.);
#2792=ORIENTED_EDGE('',*,*,#2033,.F.);
#2793=ORIENTED_EDGE('',*,*,#2034,.F.);
#2794=ORIENTED_EDGE('',*,*,#2033,.T.);
#2795=ORIENTED_EDGE('',*,*,#2035,.F.);
#2796=ORIENTED_EDGE('',*,*,#2036,.F.);
#2797=ORIENTED_EDGE('',*,*,#2037,.T.);
#2798=ORIENTED_EDGE('',*,*,#2035,.T.);
#2799=ORIENTED_EDGE('',*,*,#2032,.T.);
#2800=ORIENTED_EDGE('',*,*,#2029,.T.);
#2801=ORIENTED_EDGE('',*,*,#2034,.T.);
#2802=ORIENTED_EDGE('',*,*,#2038,.F.);
#2803=ORIENTED_EDGE('',*,*,#2039,.F.);
#2804=ORIENTED_EDGE('',*,*,#2040,.F.);
#2805=ORIENTED_EDGE('',*,*,#2041,.F.);
#2806=ORIENTED_EDGE('',*,*,#2042,.F.);
#2807=ORIENTED_EDGE('',*,*,#2027,.T.);
#2808=ORIENTED_EDGE('',*,*,#2031,.T.);
#2809=ORIENTED_EDGE('',*,*,#2043,.F.);
#2810=ORIENTED_EDGE('',*,*,#2044,.T.);
#2811=ORIENTED_EDGE('',*,*,#2045,.F.);
#2812=ORIENTED_EDGE('',*,*,#2044,.F.);
#2813=ORIENTED_EDGE('',*,*,#2046,.F.);
#2814=ORIENTED_EDGE('',*,*,#2047,.F.);
#2815=ORIENTED_EDGE('',*,*,#2048,.F.);
#2816=ORIENTED_EDGE('',*,*,#2049,.F.);
#2817=ORIENTED_EDGE('',*,*,#2050,.F.);
#2818=ORIENTED_EDGE('',*,*,#2051,.F.);
#2819=ORIENTED_EDGE('',*,*,#2052,.F.);
#2820=ORIENTED_EDGE('',*,*,#2053,.T.);
#2821=ORIENTED_EDGE('',*,*,#2054,.F.);
#2822=ORIENTED_EDGE('',*,*,#2053,.F.);
#2823=ORIENTED_EDGE('',*,*,#2055,.F.);
#2824=ORIENTED_EDGE('',*,*,#2047,.T.);
#2825=ORIENTED_EDGE('',*,*,#2049,.T.);
#2826=ORIENTED_EDGE('',*,*,#2056,.F.);
#2827=ORIENTED_EDGE('',*,*,#2057,.T.);
#2828=ORIENTED_EDGE('',*,*,#2058,.T.);
#2829=ORIENTED_EDGE('',*,*,#2059,.T.);
#2830=ORIENTED_EDGE('',*,*,#2060,.F.);
#2831=ORIENTED_EDGE('',*,*,#2061,.F.);
#2832=ORIENTED_EDGE('',*,*,#2062,.T.);
#2833=ORIENTED_EDGE('',*,*,#2063,.F.);
#2834=ORIENTED_EDGE('',*,*,#2064,.F.);
#2835=ORIENTED_EDGE('',*,*,#2057,.F.);
#2836=ORIENTED_EDGE('',*,*,#2065,.F.);
#2837=ORIENTED_EDGE('',*,*,#2066,.T.);
#2838=ORIENTED_EDGE('',*,*,#2067,.T.);
#2839=ORIENTED_EDGE('',*,*,#2068,.F.);
#2840=ORIENTED_EDGE('',*,*,#2063,.T.);
#2841=ORIENTED_EDGE('',*,*,#2069,.T.);
#2842=ORIENTED_EDGE('',*,*,#2066,.F.);
#2843=ORIENTED_EDGE('',*,*,#2070,.F.);
#2844=ORIENTED_EDGE('',*,*,#2058,.F.);
#2845=ORIENTED_EDGE('',*,*,#2067,.F.);
#2846=ORIENTED_EDGE('',*,*,#2069,.F.);
#2847=ORIENTED_EDGE('',*,*,#2062,.F.);
#2848=ORIENTED_EDGE('',*,*,#2071,.F.);
#2849=ORIENTED_EDGE('',*,*,#2072,.T.);
#2850=ORIENTED_EDGE('',*,*,#2073,.F.);
#2851=ORIENTED_EDGE('',*,*,#2074,.F.);
#2852=ORIENTED_EDGE('',*,*,#2043,.T.);
#2853=ORIENTED_EDGE('',*,*,#2051,.T.);
#2854=ORIENTED_EDGE('',*,*,#2075,.F.);
#2855=ORIENTED_EDGE('',*,*,#2072,.F.);
#2856=ORIENTED_EDGE('',*,*,#2076,.F.);
#2857=ORIENTED_EDGE('',*,*,#2077,.T.);
#2858=ORIENTED_EDGE('',*,*,#2078,.F.);
#2859=ORIENTED_EDGE('',*,*,#2041,.T.);
#2860=ORIENTED_EDGE('',*,*,#2079,.F.);
#2861=ORIENTED_EDGE('',*,*,#2045,.T.);
#2862=ORIENTED_EDGE('',*,*,#2080,.T.);
#2863=ORIENTED_EDGE('',*,*,#2081,.T.);
#2864=ORIENTED_EDGE('',*,*,#2038,.T.);
#2865=ORIENTED_EDGE('',*,*,#2036,.T.);
#2866=ORIENTED_EDGE('',*,*,#2037,.F.);
#2867=ORIENTED_EDGE('',*,*,#2028,.F.);
#2868=ORIENTED_EDGE('',*,*,#2042,.T.);
#2869=ORIENTED_EDGE('',*,*,#2078,.T.);
#2870=ORIENTED_EDGE('',*,*,#2082,.T.);
#2871=ORIENTED_EDGE('',*,*,#2073,.T.);
#2872=ORIENTED_EDGE('',*,*,#2075,.T.);
#2873=ORIENTED_EDGE('',*,*,#2050,.T.);
#2874=ORIENTED_EDGE('',*,*,#2054,.T.);
#2875=ORIENTED_EDGE('',*,*,#2046,.T.);
#2876=ORIENTED_EDGE('',*,*,#2060,.T.);
#2877=ORIENTED_EDGE('',*,*,#2083,.T.);
#2878=ORIENTED_EDGE('',*,*,#2074,.T.);
#2879=ORIENTED_EDGE('',*,*,#2082,.F.);
#2880=ORIENTED_EDGE('',*,*,#2077,.F.);
#2881=ORIENTED_EDGE('',*,*,#2084,.F.);
#2882=ORIENTED_EDGE('',*,*,#2085,.T.);
#2883=ORIENTED_EDGE('',*,*,#2064,.T.);
#2884=ORIENTED_EDGE('',*,*,#2068,.T.);
#2885=ORIENTED_EDGE('',*,*,#2065,.T.);
#2886=ORIENTED_EDGE('',*,*,#2056,.T.);
#2887=ORIENTED_EDGE('',*,*,#2048,.T.);
#2888=ORIENTED_EDGE('',*,*,#2055,.T.);
#2889=ORIENTED_EDGE('',*,*,#2052,.T.);
#2890=ORIENTED_EDGE('',*,*,#2076,.T.);
#2891=ORIENTED_EDGE('',*,*,#2071,.T.);
#2892=ORIENTED_EDGE('',*,*,#2084,.T.);
#2893=ORIENTED_EDGE('',*,*,#2079,.T.);
#2894=ORIENTED_EDGE('',*,*,#2040,.T.);
#2895=ORIENTED_EDGE('',*,*,#2086,.T.);
#2896=ORIENTED_EDGE('',*,*,#2087,.T.);
#2897=ORIENTED_EDGE('',*,*,#2083,.F.);
#2898=ORIENTED_EDGE('',*,*,#2059,.F.);
#2899=ORIENTED_EDGE('',*,*,#2070,.T.);
#2900=ORIENTED_EDGE('',*,*,#2088,.T.);
#2901=ORIENTED_EDGE('',*,*,#2086,.F.);
#2902=ORIENTED_EDGE('',*,*,#2039,.T.);
#2903=ORIENTED_EDGE('',*,*,#2081,.F.);
#2904=ORIENTED_EDGE('',*,*,#2080,.F.);
#2905=ORIENTED_EDGE('',*,*,#2087,.F.);
#2906=ORIENTED_EDGE('',*,*,#2061,.T.);
#2907=ORIENTED_EDGE('',*,*,#2085,.F.);
#2908=ORIENTED_EDGE('',*,*,#2088,.F.);
#3199=CYLINDRICAL_SURFACE('',#3786,2.5);
#3200=CYLINDRICAL_SURFACE('',#3799,4.99999999999999);
#3201=CYLINDRICAL_SURFACE('',#3807,4.99999999999999);
#3320=ADVANCED_FACE('',(#378),#199,.T.);
#3321=ADVANCED_FACE('',(#379),#200,.T.);
#3322=ADVANCED_FACE('',(#380),#201,.T.);
#3323=ADVANCED_FACE('',(#381),#202,.T.);
#3324=ADVANCED_FACE('',(#382),#203,.F.);
#3325=ADVANCED_FACE('',(#383),#3199,.F.);
#3326=ADVANCED_FACE('',(#384),#204,.F.);
#3327=ADVANCED_FACE('',(#385),#205,.F.);
#3328=ADVANCED_FACE('',(#386),#206,.F.);
#3329=ADVANCED_FACE('',(#387),#207,.F.);
#3330=ADVANCED_FACE('',(#388),#208,.F.);
#3331=ADVANCED_FACE('',(#389),#209,.F.);
#3332=ADVANCED_FACE('',(#390),#210,.F.);
#3333=ADVANCED_FACE('',(#391),#211,.F.);
#3334=ADVANCED_FACE('',(#392,#115),#212,.F.);
#3335=ADVANCED_FACE('',(#393),#3200,.F.);
#3336=ADVANCED_FACE('',(#394,#116),#213,.T.);
#3337=ADVANCED_FACE('',(#395),#214,.F.);
#3338=ADVANCED_FACE('',(#396),#215,.F.);
#3339=ADVANCED_FACE('',(#397),#216,.T.);
#3340=ADVANCED_FACE('',(#398),#3201,.F.);
#3341=ADVANCED_FACE('',(#399),#217,.T.);
#3342=ADVANCED_FACE('',(#400),#218,.F.);
#3402=CLOSED_SHELL('',(#3320,#3321,#3322,#3323,#3324,#3325,#3326,#3327,
#3328,#3329,#3330,#3331,#3332,#3333,#3334,#3335,#3336,#3337,#3338,#3339,
#3340,#3341,#3342));
#3780=AXIS2_PLACEMENT_3D('',#5742,#4538,#4539);
#3781=AXIS2_PLACEMENT_3D('',#5743,#4540,#4541);
#3782=AXIS2_PLACEMENT_3D('',#5752,#4546,#4547);
#3783=AXIS2_PLACEMENT_3D('',#5758,#4551,#4552);
#3784=AXIS2_PLACEMENT_3D('',#5764,#4556,#4557);
#3785=AXIS2_PLACEMENT_3D('',#5766,#4559,#4560);
#3786=AXIS2_PLACEMENT_3D('',#5776,#4566,#4567);
#3787=AXIS2_PLACEMENT_3D('',#5778,#4568,#4569);
#3788=AXIS2_PLACEMENT_3D('',#5781,#4571,#4572);
#3789=AXIS2_PLACEMENT_3D('',#5782,#4573,#4574);
#3790=AXIS2_PLACEMENT_3D('',#5791,#4579,#4580);
#3791=AXIS2_PLACEMENT_3D('',#5800,#4585,#4586);
#3792=AXIS2_PLACEMENT_3D('',#5803,#4589,#4590);
#3793=AXIS2_PLACEMENT_3D('',#5813,#4596,#4597);
#3794=AXIS2_PLACEMENT_3D('',#5822,#4602,#4603);
#3795=AXIS2_PLACEMENT_3D('',#5828,#4607,#4608);
#3796=AXIS2_PLACEMENT_3D('',#5831,#4611,#4612);
#3797=AXIS2_PLACEMENT_3D('',#5832,#4613,#4614);
#3798=AXIS2_PLACEMENT_3D('',#5833,#4615,#4616);
#3799=AXIS2_PLACEMENT_3D('',#5842,#4621,#4622);
#3800=AXIS2_PLACEMENT_3D('',#5843,#4623,#4624);
#3801=AXIS2_PLACEMENT_3D('',#5844,#4625,#4626);
#3802=AXIS2_PLACEMENT_3D('',#5845,#4627,#4628);
#3803=AXIS2_PLACEMENT_3D('',#5851,#4632,#4633);
#3804=AXIS2_PLACEMENT_3D('',#5857,#4637,#4638);
#3805=AXIS2_PLACEMENT_3D('',#5858,#4639,#4640);
#3806=AXIS2_PLACEMENT_3D('',#5860,#4642,#4643);
#3807=AXIS2_PLACEMENT_3D('',#5864,#4646,#4647);
#3808=AXIS2_PLACEMENT_3D('',#5866,#4649,#4650);
#3809=AXIS2_PLACEMENT_3D('',#5868,#4652,#4653);
#4538=DIRECTION('axis',(0.,0.,1.));
#4539=DIRECTION('refdir',(1.,0.,0.));
#4540=DIRECTION('center_axis',(0.,1.,0.));
#4541=DIRECTION('ref_axis',(0.,0.,-1.));
#4542=DIRECTION('',(0.,0.,1.));
#4543=DIRECTION('',(-1.,0.,0.));
#4544=DIRECTION('',(0.,0.,-1.));
#4545=DIRECTION('',(-1.,0.,0.));
#4546=DIRECTION('center_axis',(0.,0.,1.));
#4547=DIRECTION('ref_axis',(0.,1.,0.));
#4548=DIRECTION('',(0.,-1.,0.));
#4549=DIRECTION('',(0.,1.,0.));
#4550=DIRECTION('',(-1.,0.,0.));
#4551=DIRECTION('center_axis',(0.,-1.,0.));
#4552=DIRECTION('ref_axis',(0.,0.,1.));
#4553=DIRECTION('',(0.,0.,-1.));
#4554=DIRECTION('',(0.,0.,1.));
#4555=DIRECTION('',(-1.,0.,0.));
#4556=DIRECTION('center_axis',(-1.,0.,0.));
#4557=DIRECTION('ref_axis',(0.,0.,1.));
#4558=DIRECTION('',(0.,-1.,0.));
#4559=DIRECTION('center_axis',(1.,0.,0.));
#4560=DIRECTION('ref_axis',(0.,-1.,0.));
#4561=DIRECTION('',(0.,1.,0.));
#4562=DIRECTION('',(0.,0.,-1.));
#4563=DIRECTION('',(0.,-1.,0.));
#4564=DIRECTION('',(0.,0.,1.));
#4565=DIRECTION('',(0.,1.,0.));
#4566=DIRECTION('center_axis',(0.,1.,0.));
#4567=DIRECTION('ref_axis',(1.,0.,0.));
#4568=DIRECTION('center_axis',(0.,1.,0.));
#4569=DIRECTION('ref_axis',(1.,0.,0.));
#4570=DIRECTION('',(0.,1.,0.));
#4571=DIRECTION('center_axis',(0.,-1.,0.));
#4572=DIRECTION('ref_axis',(1.,0.,0.));
#4573=DIRECTION('center_axis',(0.,-1.,0.));
#4574=DIRECTION('ref_axis',(-1.,0.,0.));
#4575=DIRECTION('',(1.,0.,0.));
#4576=DIRECTION('',(0.,0.,-1.));
#4577=DIRECTION('',(-1.,0.,0.));
#4578=DIRECTION('',(0.,0.,1.));
#4579=DIRECTION('center_axis',(0.,1.,0.));
#4580=DIRECTION('ref_axis',(1.,0.,0.));
#4581=DIRECTION('',(-1.,0.,0.));
#4582=DIRECTION('',(0.,0.,-1.));
#4583=DIRECTION('',(1.,0.,0.));
#4584=DIRECTION('',(0.,0.,-1.));
#4585=DIRECTION('center_axis',(-1.,0.,0.));
#4586=DIRECTION('ref_axis',(0.,1.,0.));
#4587=DIRECTION('',(0.,-1.,0.));
#4588=DIRECTION('',(0.,1.,0.));
#4589=DIRECTION('center_axis',(-1.,0.,0.));
#4590=DIRECTION('ref_axis',(0.,1.,0.));
#4591=DIRECTION('',(0.,1.,0.));
#4592=DIRECTION('',(0.,0.,-1.));
#4593=DIRECTION('',(0.,-1.,0.));
#4594=DIRECTION('',(0.,0.,-1.));
#4595=DIRECTION('',(0.,-1.,0.));
#4596=DIRECTION('center_axis',(0.,-1.,0.));
#4597=DIRECTION('ref_axis',(-1.,0.,0.));
#4598=DIRECTION('',(0.,0.,1.));
#4599=DIRECTION('',(-1.,0.,0.));
#4600=DIRECTION('',(0.,0.,-1.));
#4601=DIRECTION('',(-1.,0.,0.));
#4602=DIRECTION('center_axis',(0.,1.,0.));
#4603=DIRECTION('ref_axis',(1.,0.,0.));
#4604=DIRECTION('',(1.,0.,0.));
#4605=DIRECTION('',(0.,0.,-1.));
#4606=DIRECTION('',(1.,0.,0.));
#4607=DIRECTION('center_axis',(-1.,0.,0.));
#4608=DIRECTION('ref_axis',(0.,1.,0.));
#4609=DIRECTION('',(0.,1.,0.));
#4610=DIRECTION('',(0.,1.,0.));
#4611=DIRECTION('center_axis',(0.,0.,-1.));
#4612=DIRECTION('ref_axis',(-1.,0.,0.));
#4613=DIRECTION('center_axis',(0.,0.,1.));
#4614=DIRECTION('ref_axis',(-1.,8.88178419700126E-16,0.));
#4615=DIRECTION('center_axis',(0.,1.,0.));
#4616=DIRECTION('ref_axis',(1.,0.,0.));
#4617=DIRECTION('',(1.,0.,0.));
#4618=DIRECTION('',(0.,0.,-1.));
#4619=DIRECTION('',(-1.,0.,0.));
#4620=DIRECTION('',(0.,0.,-1.));
#4621=DIRECTION('center_axis',(0.,0.,-1.));
#4622=DIRECTION('ref_axis',(1.33226762955019E-15,1.,0.));
#4623=DIRECTION('center_axis',(0.,0.,1.));
#4624=DIRECTION('ref_axis',(1.33226762955019E-15,1.,0.));
#4625=DIRECTION('center_axis',(0.,0.,-1.));
#4626=DIRECTION('ref_axis',(1.33226762955019E-15,1.,0.));
#4627=DIRECTION('center_axis',(0.,1.,0.));
#4628=DIRECTION('ref_axis',(-1.,0.,0.));
#4629=DIRECTION('',(0.,0.,-1.));
#4630=DIRECTION('',(1.,0.,0.));
#4631=DIRECTION('',(-1.,0.,0.));
#4632=DIRECTION('center_axis',(0.,0.,1.));
#4633=DIRECTION('ref_axis',(1.,0.,0.));
#4634=DIRECTION('',(0.,-1.,0.));
#4635=DIRECTION('',(-1.,0.,0.));
#4636=DIRECTION('',(0.,-1.,0.));
#4637=DIRECTION('center_axis',(0.,0.,1.));
#4638=DIRECTION('ref_axis',(-1.,8.88178419700126E-16,0.));
#4639=DIRECTION('center_axis',(-1.,0.,0.));
#4640=DIRECTION('ref_axis',(0.,1.,0.));
#4641=DIRECTION('',(0.,1.,0.));
#4642=DIRECTION('center_axis',(0.,0.,1.));
#4643=DIRECTION('ref_axis',(1.,0.,0.));
#4644=DIRECTION('',(0.,1.,0.));
#4645=DIRECTION('',(1.,0.,0.));
#4646=DIRECTION('center_axis',(0.,0.,-1.));
#4647=DIRECTION('ref_axis',(-1.,8.88178419700126E-16,0.));
#4648=DIRECTION('',(0.,0.,-1.));
#4649=DIRECTION('center_axis',(0.,-1.,0.));
#4650=DIRECTION('ref_axis',(1.,0.,0.));
#4651=DIRECTION('',(0.,0.,1.));
#4652=DIRECTION('center_axis',(-1.,0.,0.));
#4653=DIRECTION('ref_axis',(0.,1.,0.));
#5742=CARTESIAN_POINT('',(0.,0.,0.));
#5743=CARTESIAN_POINT('Origin',(-29.1374542444053,4.,6.));
#5744=CARTESIAN_POINT('',(-29.1374542444053,4.,0.));
#5745=CARTESIAN_POINT('',(-29.1374542444053,4.,6.));
#5746=CARTESIAN_POINT('',(-29.1374542444053,4.,11.));
#5747=CARTESIAN_POINT('',(-35.1374542444053,4.,0.));
#5748=CARTESIAN_POINT('',(-29.1374542444053,4.,0.));
#5749=CARTESIAN_POINT('',(-35.1374542444053,4.,6.));
#5750=CARTESIAN_POINT('',(-35.1374542444053,4.,6.));
#5751=CARTESIAN_POINT('',(-29.1374542444053,4.,6.));
#5752=CARTESIAN_POINT('Origin',(-29.1374542444053,-4.,6.));
#5753=CARTESIAN_POINT('',(-29.1374542444053,-4.,6.));
#5754=CARTESIAN_POINT('',(-29.1374542444053,13.,6.));
#5755=CARTESIAN_POINT('',(-35.1374542444053,-4.,6.));
#5756=CARTESIAN_POINT('',(-35.1374542444053,-4.,6.));
#5757=CARTESIAN_POINT('',(-29.1374542444053,-4.,6.));
#5758=CARTESIAN_POINT('Origin',(-29.1374542444053,-4.,0.));
#5759=CARTESIAN_POINT('',(-29.1374542444053,-4.,0.));
#5760=CARTESIAN_POINT('',(-29.1374542444053,-4.,8.));
#5761=CARTESIAN_POINT('',(-35.1374542444053,-4.,0.));
#5762=CARTESIAN_POINT('',(-35.1374542444053,-4.,-6.));
#5763=CARTESIAN_POINT('',(-29.1374542444053,-4.,0.));
#5764=CARTESIAN_POINT('Origin',(-35.1374542444053,0.,3.));
#5765=CARTESIAN_POINT('',(-35.1374542444053,30.,0.));
#5766=CARTESIAN_POINT('Origin',(-29.1374542444053,30.,16.));
#5767=CARTESIAN_POINT('',(-29.1374542444053,-30.,0.));
#5768=CARTESIAN_POINT('',(-29.1374542444053,15.,0.));
#5769=CARTESIAN_POINT('',(-29.1374542444053,-30.,16.));
#5770=CARTESIAN_POINT('',(-29.1374542444053,-30.,8.));
#5771=CARTESIAN_POINT('',(-29.1374542444053,30.,16.));
#5772=CARTESIAN_POINT('',(-29.1374542444053,15.,16.));
#5773=CARTESIAN_POINT('',(-29.1374542444053,30.,0.));
#5774=CARTESIAN_POINT('',(-29.1374542444053,30.,8.));
#5775=CARTESIAN_POINT('',(-29.1374542444053,15.,0.));
#5776=CARTESIAN_POINT('Origin',(-11.6523566026163,-30.,8.));
#5777=CARTESIAN_POINT('',(-14.1523566026163,15.,8.));
#5778=CARTESIAN_POINT('Origin',(-11.6523566026163,15.,8.));
#5779=CARTESIAN_POINT('',(-14.1523566026163,30.,8.));
#5780=CARTESIAN_POINT('',(-14.1523566026163,-30.,8.));
#5781=CARTESIAN_POINT('Origin',(-11.6523566026163,30.,8.));
#5782=CARTESIAN_POINT('Origin',(-17.8106534302817,8.98579659039556,16.));
#5783=CARTESIAN_POINT('',(-21.,8.98579659039556,0.));
#5784=CARTESIAN_POINT('',(-20.,8.98579659039556,0.));
#5785=CARTESIAN_POINT('',(-8.90532671514083,8.98579659039556,0.));
#5786=CARTESIAN_POINT('',(-21.,8.98579659039556,16.));
#5787=CARTESIAN_POINT('',(-21.,8.98579659039556,16.));
#5788=CARTESIAN_POINT('',(-20.,8.98579659039556,16.));
#5789=CARTESIAN_POINT('',(-8.90532671514083,8.98579659039556,16.));
#5790=CARTESIAN_POINT('',(-20.,8.98579659039556,16.));
#5791=CARTESIAN_POINT('Origin',(-21.,13.1380156428221,16.));
#5792=CARTESIAN_POINT('',(-18.8926671865707,13.1380156428221,0.));
#5793=CARTESIAN_POINT('',(-21.,13.1380156428221,0.));
#5794=CARTESIAN_POINT('',(-10.5,13.1380156428221,0.));
#5795=CARTESIAN_POINT('',(-18.8926671865707,13.1380156428221,16.));
#5796=CARTESIAN_POINT('',(-18.8926671865707,13.1380156428221,16.));
#5797=CARTESIAN_POINT('',(-21.,13.1380156428221,16.));
#5798=CARTESIAN_POINT('',(-10.5,13.1380156428221,16.));
#5799=CARTESIAN_POINT('',(-21.,13.1380156428221,16.));
#5800=CARTESIAN_POINT('Origin',(-21.,8.98579659039556,16.));
#5801=CARTESIAN_POINT('',(-21.,4.49289829519778,0.));
#5802=CARTESIAN_POINT('',(-21.,4.49289829519778,16.));
#5803=CARTESIAN_POINT('Origin',(-20.,-10.,16.));
#5804=CARTESIAN_POINT('',(-20.,-2.10952062437159,16.));
#5805=CARTESIAN_POINT('',(-20.,-5.,16.));
#5806=CARTESIAN_POINT('',(-20.,-2.10952062437159,14.));
#5807=CARTESIAN_POINT('',(-20.,-2.10952062437159,16.));
#5808=CARTESIAN_POINT('',(-20.,-10.,14.));
#5809=CARTESIAN_POINT('',(-20.,-8.5547603121858,14.));
#5810=CARTESIAN_POINT('',(-20.,-10.,0.));
#5811=CARTESIAN_POINT('',(-20.,-10.,16.));
#5812=CARTESIAN_POINT('',(-20.,-5.,0.));
#5813=CARTESIAN_POINT('Origin',(25.,-12.1095206243716,16.));
#5814=CARTESIAN_POINT('',(-19.5332022605826,-12.1095206243716,14.));
#5815=CARTESIAN_POINT('',(-19.5332022605826,-12.1095206243716,16.));
#5816=CARTESIAN_POINT('',(-19.5332022605826,-12.1095206243716,16.));
#5817=CARTESIAN_POINT('',(-25.,-12.1095206243716,14.));
#5818=CARTESIAN_POINT('',(-25.,-12.1095206243716,14.));
#5819=CARTESIAN_POINT('',(-25.,-12.1095206243716,16.));
#5820=CARTESIAN_POINT('',(-25.,-12.1095206243716,16.));
#5821=CARTESIAN_POINT('',(12.5,-12.1095206243716,16.));
#5822=CARTESIAN_POINT('Origin',(-25.,-2.10952062437159,16.));
#5823=CARTESIAN_POINT('',(-25.,-2.10952062437159,16.));
#5824=CARTESIAN_POINT('',(-12.5,-2.10952062437159,16.));
#5825=CARTESIAN_POINT('',(-25.,-2.10952062437159,14.));
#5826=CARTESIAN_POINT('',(-25.,-2.10952062437159,16.));
#5827=CARTESIAN_POINT('',(25.,-2.10952062437159,14.));
#5828=CARTESIAN_POINT('Origin',(-25.,-12.1095206243716,16.));
#5829=CARTESIAN_POINT('',(-25.,-6.0547603121858,16.));
#5830=CARTESIAN_POINT('',(-25.,-2.10952062437159,14.));
#5831=CARTESIAN_POINT('Origin',(0.,-7.10952062437159,14.));
#5832=CARTESIAN_POINT('Origin',(-15.,-10.,14.));
#5833=CARTESIAN_POINT('Origin',(-15.,15.,16.));
#5834=CARTESIAN_POINT('',(-15.,15.,16.));
#5835=CARTESIAN_POINT('',(29.1374542444053,15.,16.));
#5836=CARTESIAN_POINT('',(7.5,15.,16.));
#5837=CARTESIAN_POINT('',(-15.,15.,0.));
#5838=CARTESIAN_POINT('',(-15.,15.,16.));
#5839=CARTESIAN_POINT('',(29.1374542444053,15.,0.));
#5840=CARTESIAN_POINT('',(7.5,15.,0.));
#5841=CARTESIAN_POINT('',(29.1374542444053,15.,16.));
#5842=CARTESIAN_POINT('Origin',(-15.,10.,16.));
#5843=CARTESIAN_POINT('Origin',(-15.,10.,0.));
#5844=CARTESIAN_POINT('Origin',(-15.,10.,16.));
#5845=CARTESIAN_POINT('Origin',(50.,30.,0.));
#5846=CARTESIAN_POINT('',(29.1374542444053,30.,16.));
#5847=CARTESIAN_POINT('',(29.1374542444053,30.,0.));
#5848=CARTESIAN_POINT('',(29.1374542444053,30.,8.));
#5849=CARTESIAN_POINT('',(-50.,30.,0.));
#5850=CARTESIAN_POINT('',(-50.,30.,16.));
#5851=CARTESIAN_POINT('Origin',(0.,0.,0.));
#5852=CARTESIAN_POINT('',(-19.5332022605826,-12.1095206243716,0.));
#5853=CARTESIAN_POINT('',(-19.5332022605826,-30.,0.));
#5854=CARTESIAN_POINT('',(-19.5332022605826,-15.,0.));
#5855=CARTESIAN_POINT('',(50.,-30.,0.));
#5856=CARTESIAN_POINT('',(29.1374542444053,-15.,0.));
#5857=CARTESIAN_POINT('Origin',(-15.,-10.,0.));
#5858=CARTESIAN_POINT('Origin',(29.1374542444053,-30.,16.));
#5859=CARTESIAN_POINT('',(29.1374542444053,-15.,16.));
#5860=CARTESIAN_POINT('Origin',(0.,0.,16.));
#5861=CARTESIAN_POINT('',(-19.5332022605826,-30.,16.));
#5862=CARTESIAN_POINT('',(-19.5332022605826,-15.,16.));
#5863=CARTESIAN_POINT('',(50.,-30.,16.));
#5864=CARTESIAN_POINT('Origin',(-15.,-10.,16.));
#5865=CARTESIAN_POINT('',(-19.5332022605826,-12.1095206243716,16.));
#5866=CARTESIAN_POINT('Origin',(-50.,-30.,0.));
#5867=CARTESIAN_POINT('',(-19.5332022605826,-30.,8.));
#5868=CARTESIAN_POINT('Origin',(-19.5332022605826,-30.,16.));
#7030=UNCERTAINTY_MEASURE_WITH_UNIT(LENGTH_MEASURE(0.01),#7048,
'DISTANCE_ACCURACY_VALUE',
'Maximum model space distance between geometric entities at asserted c
onnectivities');
#7035=UNCERTAINTY_MEASURE_WITH_UNIT(LENGTH_MEASURE(0.01),#7048,
'DISTANCE_ACCURACY_VALUE',
'Maximum model space distance between geometric entities at asserted c
onnectivities');
#7042=(
GEOMETRIC_REPRESENTATION_CONTEXT(3)
GLOBAL_UNCERTAINTY_ASSIGNED_CONTEXT((#7030))
GLOBAL_UNIT_ASSIGNED_CONTEXT((#7048,#7050,#7051))
REPRESENTATION_CONTEXT('','3D')
);
#7047=(
GEOMETRIC_REPRESENTATION_CONTEXT(3)
GLOBAL_UNCERTAINTY_ASSIGNED_CONTEXT((#7035))
GLOBAL_UNIT_ASSIGNED_CONTEXT((#7048,#7050,#7051))
REPRESENTATION_CONTEXT('','3D')
);
#7048=(
LENGTH_UNIT()
NAMED_UNIT(*)
SI_UNIT(.MILLI.,.METRE.)
);
#7050=(
NAMED_UNIT(*)
PLANE_ANGLE_UNIT()
SI_UNIT($,.RADIAN.)
);
#7051=(
NAMED_UNIT(*)
SI_UNIT($,.STERADIAN.)
SOLID_ANGLE_UNIT()
);
#7058=SHAPE_DEFINITION_REPRESENTATION(#7069,#7090);
#7069=PRODUCT_DEFINITION_SHAPE('',$,#7102);
#7090=SHAPE_REPRESENTATION('',(#3780),#7042);
#7095=PRODUCT_DEFINITION_CONTEXT('part definition',#7130,'design');
#7102=PRODUCT_DEFINITION('Left_Block','Left_Block',#7113,#7095);
#7113=PRODUCT_DEFINITION_FORMATION('',$,#7138);
#7130=APPLICATION_CONTEXT(
'Core Data for Automotive Mechanical Design Process');
#7131=PRODUCT_CONTEXT('part definition',#7130,'mechanical');
#7138=PRODUCT('Left_Block','Left_Block',$,(#7131));
#7171=COLOUR_RGB('Dark Blue',0.08,0.2,0.34);
#7172=FILL_AREA_STYLE_COLOUR('',#7171);
#7173=FILL_AREA_STYLE('',(#7172));
#7174=SURFACE_STYLE_FILL_AREA(#7173);
#7175=SURFACE_SIDE_STYLE('',(#7174));
#7176=SURFACE_STYLE_USAGE(.BOTH.,#7175);
#7177=PRESENTATION_STYLE_ASSIGNMENT((#7176));
ENDSEC;
END-ISO-10303-21;
